ISO-10303-21;
HEADER;
/* Generated by software containing ST-Developer
 * from STEP Tools, Inc. (www.steptools.com) 
 */

FILE_DESCRIPTION(
/* description */ ('Belt-driven linear axis on 2020 extrusion'),
/* implementation_level */ '2;1');

FILE_NAME(
/* name */ 'Cap Screw - M4x16.step',
/* time_stamp */ '2026-10-28T03:26:09-07:00',
/* author */ (''),
/* organization */ (''),
/* preprocessor_version */ 'ST-DEVELOPER v20.2',
/* originating_system */ 'Autodesk Translation Framework v15.17.0.0',
/* authorisation */ '');

FILE_SCHEMA (('AUTOMOTIVE_DESIGN { 1 0 10303 214 3 1 1 }'));
ENDSEC;

DATA;
#10=MECHANICAL_DESIGN_GEOMETRIC_PRESENTATION_REPRESENTATION('',(#665),#20096);
#14=ORIENTED_CLOSED_SHELL('',*,#10982,.F.);
#18=BREP_WITH_VOIDS('Body1',#10981,(#14));
#512=CONICAL_SURFACE('',#12665,0.325,0.785398163397448);
#513=CONICAL_SURFACE('',#12669,0.335,0.785398163397448);
#514=CONICAL_SURFACE('',#12673,0.21,0.463647609000806);
#515=CONICAL_SURFACE('',#12677,0.18,0.785398163397448);
#563=SHAPE_REPRESENTATION_RELATIONSHIP('SRR','None',#20364,#609);
#609=ADVANCED_BREP_SHAPE_REPRESENTATION('',(#18),#20095);
#665=STYLED_ITEM('',(#20657),#18);
#888=FACE_BOUND('',#2652,.T.);
#1239=PLANE('',#12663);
#1240=PLANE('',#12671);
#1241=PLANE('',#12679);
#1242=PLANE('',#12680);
#1243=PLANE('',#12681);
#1244=PLANE('',#12682);
#1245=PLANE('',#12683);
#1246=PLANE('',#12684);
#1247=PLANE('',#12685);
#1248=PLANE('',#12686);
#1249=PLANE('',#12687);
#1855=FACE_OUTER_BOUND('',#2647,.T.);
#1856=FACE_OUTER_BOUND('',#2648,.T.);
#1857=FACE_OUTER_BOUND('',#2649,.T.);
#1858=FACE_OUTER_BOUND('',#2650,.T.);
#1859=FACE_OUTER_BOUND('',#2651,.T.);
#1860=FACE_OUTER_BOUND('',#2653,.T.);
#1861=FACE_OUTER_BOUND('',#2654,.T.);
#1862=FACE_OUTER_BOUND('',#2655,.T.);
#1863=FACE_OUTER_BOUND('',#2656,.T.);
#1864=FACE_OUTER_BOUND('',#2657,.T.);
#1865=FACE_OUTER_BOUND('',#2658,.T.);
#1866=FACE_OUTER_BOUND('',#2659,.T.);
#1867=FACE_OUTER_BOUND('',#2660,.T.);
#1868=FACE_OUTER_BOUND('',#2661,.T.);
#1869=FACE_OUTER_BOUND('',#2662,.T.);
#1870=FACE_OUTER_BOUND('',#2663,.T.);
#1871=FACE_OUTER_BOUND('',#2664,.T.);
#2647=EDGE_LOOP('',(#10013));
#2648=EDGE_LOOP('',(#10014,#10015,#10016,#10017));
#2649=EDGE_LOOP('',(#10018,#10019,#10020,#10021));
#2650=EDGE_LOOP('',(#10022,#10023,#10024,#10025));
#2651=EDGE_LOOP('',(#10026));
#2652=EDGE_LOOP('',(#10027));
#2653=EDGE_LOOP('',(#10028,#10029,#10030,#10031));
#2654=EDGE_LOOP('',(#10032,#10033,#10034,#10035));
#2655=EDGE_LOOP('',(#10036,#10037,#10038,#10039));
#2656=EDGE_LOOP('',(#10040));
#2657=EDGE_LOOP('',(#10041,#10042,#10043,#10044));
#2658=EDGE_LOOP('',(#10045,#10046,#10047,#10048));
#2659=EDGE_LOOP('',(#10049,#10050,#10051,#10052));
#2660=EDGE_LOOP('',(#10053,#10054,#10055,#10056));
#2661=EDGE_LOOP('',(#10057,#10058,#10059,#10060));
#2662=EDGE_LOOP('',(#10061,#10062,#10063,#10064));
#2663=EDGE_LOOP('',(#10065,#10066,#10067,#10068,#10069,#10070));
#2664=EDGE_LOOP('',(#10071,#10072,#10073,#10074,#10075,#10076));
#3498=LINE('',#19829,#4355);
#3499=LINE('',#19833,#4356);
#3500=LINE('',#19837,#4357);
#3501=LINE('',#19844,#4358);
#3502=LINE('',#19848,#4359);
#3503=LINE('',#19852,#4360);
#3504=LINE('',#19857,#4361);
#3505=LINE('',#19859,#4362);
#3506=LINE('',#19861,#4363);
#3507=LINE('',#19862,#4364);
#3508=LINE('',#19865,#4365);
#3509=LINE('',#19867,#4366);
#3510=LINE('',#19868,#4367);
#3511=LINE('',#19871,#4368);
#3512=LINE('',#19873,#4369);
#3513=LINE('',#19874,#4370);
#3514=LINE('',#19877,#4371);
#3515=LINE('',#19879,#4372);
#3516=LINE('',#19880,#4373);
#3517=LINE('',#19883,#4374);
#3518=LINE('',#19885,#4375);
#3519=LINE('',#19886,#4376);
#3520=LINE('',#19888,#4377);
#3521=LINE('',#19889,#4378);
#4355=VECTOR('',#15972,0.325);
#4356=VECTOR('',#15977,0.35);
#4357=VECTOR('',#15982,0.335);
#4358=VECTOR('',#15991,0.21);
#4359=VECTOR('',#15996,0.2);
#4360=VECTOR('',#16001,0.18);
#4361=VECTOR('',#16006,1.);
#4362=VECTOR('',#16007,1.);
#4363=VECTOR('',#16008,1.);
#4364=VECTOR('',#16009,1.);
#4365=VECTOR('',#16012,1.);
#4366=VECTOR('',#16013,1.);
#4367=VECTOR('',#16014,1.);
#4368=VECTOR('',#16017,1.);
#4369=VECTOR('',#16018,1.);
#4370=VECTOR('',#16019,1.);
#4371=VECTOR('',#16022,1.);
#4372=VECTOR('',#16023,1.);
#4373=VECTOR('',#16024,1.);
#4374=VECTOR('',#16027,1.);
#4375=VECTOR('',#16028,1.);
#4376=VECTOR('',#16029,1.);
#4377=VECTOR('',#16032,1.);
#4378=VECTOR('',#16033,1.);
#4884=CIRCLE('',#12664,0.3);
#4885=CIRCLE('',#12666,0.35);
#4886=CIRCLE('',#12668,0.35);
#4887=CIRCLE('',#12670,0.32);
#4888=CIRCLE('',#12672,0.22);
#4889=CIRCLE('',#12674,0.1954);
#4890=CIRCLE('',#12676,0.1954);
#4891=CIRCLE('',#12678,0.16);
#5821=VERTEX_POINT('',#19824);
#5822=VERTEX_POINT('',#19827);
#5823=VERTEX_POINT('',#19831);
#5824=VERTEX_POINT('',#19835);
#5825=VERTEX_POINT('',#19839);
#5826=VERTEX_POINT('',#19842);
#5827=VERTEX_POINT('',#19846);
#5828=VERTEX_POINT('',#19850);
#5829=VERTEX_POINT('',#19855);
#5830=VERTEX_POINT('',#19856);
#5831=VERTEX_POINT('',#19858);
#5832=VERTEX_POINT('',#19860);
#5833=VERTEX_POINT('',#19864);
#5834=VERTEX_POINT('',#19866);
#5835=VERTEX_POINT('',#19870);
#5836=VERTEX_POINT('',#19872);
#5837=VERTEX_POINT('',#19876);
#5838=VERTEX_POINT('',#19878);
#5839=VERTEX_POINT('',#19882);
#5840=VERTEX_POINT('',#19884);
#7221=EDGE_CURVE('',#5821,#5821,#4884,.T.);
#7222=EDGE_CURVE('',#5822,#5822,#4885,.T.);
#7223=EDGE_CURVE('',#5822,#5821,#3498,.T.);
#7224=EDGE_CURVE('',#5823,#5823,#4886,.T.);
#7225=EDGE_CURVE('',#5823,#5822,#3499,.T.);
#7226=EDGE_CURVE('',#5824,#5824,#4887,.T.);
#7227=EDGE_CURVE('',#5824,#5823,#3500,.T.);
#7228=EDGE_CURVE('',#5825,#5825,#4888,.T.);
#7229=EDGE_CURVE('',#5826,#5826,#4889,.F.);
#7230=EDGE_CURVE('',#5826,#5825,#3501,.T.);
#7231=EDGE_CURVE('',#5827,#5827,#4890,.F.);
#7232=EDGE_CURVE('',#5827,#5826,#3502,.T.);
#7233=EDGE_CURVE('',#5828,#5828,#4891,.T.);
#7234=EDGE_CURVE('',#5828,#5827,#3503,.T.);
#7235=EDGE_CURVE('',#5829,#5830,#3504,.T.);
#7236=EDGE_CURVE('',#5830,#5831,#3505,.T.);
#7237=EDGE_CURVE('',#5831,#5832,#3506,.T.);
#7238=EDGE_CURVE('',#5829,#5832,#3507,.T.);
#7239=EDGE_CURVE('',#5830,#5833,#3508,.T.);
#7240=EDGE_CURVE('',#5833,#5834,#3509,.T.);
#7241=EDGE_CURVE('',#5834,#5831,#3510,.T.);
#7242=EDGE_CURVE('',#5833,#5835,#3511,.T.);
#7243=EDGE_CURVE('',#5835,#5836,#3512,.T.);
#7244=EDGE_CURVE('',#5836,#5834,#3513,.T.);
#7245=EDGE_CURVE('',#5835,#5837,#3514,.T.);
#7246=EDGE_CURVE('',#5837,#5838,#3515,.T.);
#7247=EDGE_CURVE('',#5838,#5836,#3516,.T.);
#7248=EDGE_CURVE('',#5837,#5839,#3517,.T.);
#7249=EDGE_CURVE('',#5839,#5840,#3518,.T.);
#7250=EDGE_CURVE('',#5840,#5838,#3519,.T.);
#7251=EDGE_CURVE('',#5839,#5829,#3520,.T.);
#7252=EDGE_CURVE('',#5832,#5840,#3521,.T.);
#10013=ORIENTED_EDGE('',*,*,#7221,.F.);
#10014=ORIENTED_EDGE('',*,*,#7222,.F.);
#10015=ORIENTED_EDGE('',*,*,#7223,.T.);
#10016=ORIENTED_EDGE('',*,*,#7221,.T.);
#10017=ORIENTED_EDGE('',*,*,#7223,.F.);
#10018=ORIENTED_EDGE('',*,*,#7224,.F.);
#10019=ORIENTED_EDGE('',*,*,#7225,.T.);
#10020=ORIENTED_EDGE('',*,*,#7222,.T.);
#10021=ORIENTED_EDGE('',*,*,#7225,.F.);
#10022=ORIENTED_EDGE('',*,*,#7226,.F.);
#10023=ORIENTED_EDGE('',*,*,#7227,.T.);
#10024=ORIENTED_EDGE('',*,*,#7224,.T.);
#10025=ORIENTED_EDGE('',*,*,#7227,.F.);
#10026=ORIENTED_EDGE('',*,*,#7226,.T.);
#10027=ORIENTED_EDGE('',*,*,#7228,.F.);
#10028=ORIENTED_EDGE('',*,*,#7229,.F.);
#10029=ORIENTED_EDGE('',*,*,#7230,.T.);
#10030=ORIENTED_EDGE('',*,*,#7228,.T.);
#10031=ORIENTED_EDGE('',*,*,#7230,.F.);
#10032=ORIENTED_EDGE('',*,*,#7231,.F.);
#10033=ORIENTED_EDGE('',*,*,#7232,.T.);
#10034=ORIENTED_EDGE('',*,*,#7229,.T.);
#10035=ORIENTED_EDGE('',*,*,#7232,.F.);
#10036=ORIENTED_EDGE('',*,*,#7233,.F.);
#10037=ORIENTED_EDGE('',*,*,#7234,.T.);
#10038=ORIENTED_EDGE('',*,*,#7231,.T.);
#10039=ORIENTED_EDGE('',*,*,#7234,.F.);
#10040=ORIENTED_EDGE('',*,*,#7233,.T.);
#10041=ORIENTED_EDGE('',*,*,#7235,.T.);
#10042=ORIENTED_EDGE('',*,*,#7236,.T.);
#10043=ORIENTED_EDGE('',*,*,#7237,.T.);
#10044=ORIENTED_EDGE('',*,*,#7238,.F.);
#10045=ORIENTED_EDGE('',*,*,#7239,.T.);
#10046=ORIENTED_EDGE('',*,*,#7240,.T.);
#10047=ORIENTED_EDGE('',*,*,#7241,.T.);
#10048=ORIENTED_EDGE('',*,*,#7236,.F.);
#10049=ORIENTED_EDGE('',*,*,#7242,.T.);
#10050=ORIENTED_EDGE('',*,*,#7243,.T.);
#10051=ORIENTED_EDGE('',*,*,#7244,.T.);
#10052=ORIENTED_EDGE('',*,*,#7240,.F.);
#10053=ORIENTED_EDGE('',*,*,#7245,.T.);
#10054=ORIENTED_EDGE('',*,*,#7246,.T.);
#10055=ORIENTED_EDGE('',*,*,#7247,.T.);
#10056=ORIENTED_EDGE('',*,*,#7243,.F.);
#10057=ORIENTED_EDGE('',*,*,#7248,.T.);
#10058=ORIENTED_EDGE('',*,*,#7249,.T.);
#10059=ORIENTED_EDGE('',*,*,#7250,.T.);
#10060=ORIENTED_EDGE('',*,*,#7246,.F.);
#10061=ORIENTED_EDGE('',*,*,#7251,.T.);
#10062=ORIENTED_EDGE('',*,*,#7238,.T.);
#10063=ORIENTED_EDGE('',*,*,#7252,.T.);
#10064=ORIENTED_EDGE('',*,*,#7249,.F.);
#10065=ORIENTED_EDGE('',*,*,#7251,.F.);
#10066=ORIENTED_EDGE('',*,*,#7248,.F.);
#10067=ORIENTED_EDGE('',*,*,#7245,.F.);
#10068=ORIENTED_EDGE('',*,*,#7242,.F.);
#10069=ORIENTED_EDGE('',*,*,#7239,.F.);
#10070=ORIENTED_EDGE('',*,*,#7235,.F.);
#10071=ORIENTED_EDGE('',*,*,#7252,.F.);
#10072=ORIENTED_EDGE('',*,*,#7237,.F.);
#10073=ORIENTED_EDGE('',*,*,#7241,.F.);
#10074=ORIENTED_EDGE('',*,*,#7244,.F.);
#10075=ORIENTED_EDGE('',*,*,#7247,.F.);
#10076=ORIENTED_EDGE('',*,*,#7250,.F.);
#10299=CYLINDRICAL_SURFACE('',#12667,0.35);
#10300=CYLINDRICAL_SURFACE('',#12675,0.1954);
#10906=ADVANCED_FACE('',(#1855),#1239,.T.);
#10907=ADVANCED_FACE('',(#1856),#512,.T.);
#10908=ADVANCED_FACE('',(#1857),#10299,.T.);
#10909=ADVANCED_FACE('',(#1858),#513,.T.);
#10910=ADVANCED_FACE('',(#1859,#888),#1240,.T.);
#10911=ADVANCED_FACE('',(#1860),#514,.T.);
#10912=ADVANCED_FACE('',(#1861),#10300,.T.);
#10913=ADVANCED_FACE('',(#1862),#515,.T.);
#10914=ADVANCED_FACE('',(#1863),#1241,.T.);
#10915=ADVANCED_FACE('',(#1864),#1242,.F.);
#10916=ADVANCED_FACE('',(#1865),#1243,.F.);
#10917=ADVANCED_FACE('',(#1866),#1244,.F.);
#10918=ADVANCED_FACE('',(#1867),#1245,.F.);
#10919=ADVANCED_FACE('',(#1868),#1246,.F.);
#10920=ADVANCED_FACE('',(#1869),#1247,.F.);
#10921=ADVANCED_FACE('',(#1870),#1248,.F.);
#10922=ADVANCED_FACE('',(#1871),#1249,.F.);
#10981=CLOSED_SHELL('',(#10906,#10907,#10908,#10909,#10910,#10911,#10912,
#10913,#10914));
#10982=CLOSED_SHELL('',(#10915,#10916,#10917,#10918,#10919,#10920,#10921,
#10922));
#12662=AXIS2_PLACEMENT_3D('',#19822,#15962,#15963);
#12663=AXIS2_PLACEMENT_3D('',#19823,#15964,#15965);
#12664=AXIS2_PLACEMENT_3D('',#19825,#15966,#15967);
#12665=AXIS2_PLACEMENT_3D('',#19826,#15968,#15969);
#12666=AXIS2_PLACEMENT_3D('',#19828,#15970,#15971);
#12667=AXIS2_PLACEMENT_3D('',#19830,#15973,#15974);
#12668=AXIS2_PLACEMENT_3D('',#19832,#15975,#15976);
#12669=AXIS2_PLACEMENT_3D('',#19834,#15978,#15979);
#12670=AXIS2_PLACEMENT_3D('',#19836,#15980,#15981);
#12671=AXIS2_PLACEMENT_3D('',#19838,#15983,#15984);
#12672=AXIS2_PLACEMENT_3D('',#19840,#15985,#15986);
#12673=AXIS2_PLACEMENT_3D('',#19841,#15987,#15988);
#12674=AXIS2_PLACEMENT_3D('',#19843,#15989,#15990);
#12675=AXIS2_PLACEMENT_3D('',#19845,#15992,#15993);
#12676=AXIS2_PLACEMENT_3D('',#19847,#15994,#15995);
#12677=AXIS2_PLACEMENT_3D('',#19849,#15997,#15998);
#12678=AXIS2_PLACEMENT_3D('',#19851,#15999,#16000);
#12679=AXIS2_PLACEMENT_3D('',#19853,#16002,#16003);
#12680=AXIS2_PLACEMENT_3D('',#19854,#16004,#16005);
#12681=AXIS2_PLACEMENT_3D('',#19863,#16010,#16011);
#12682=AXIS2_PLACEMENT_3D('',#19869,#16015,#16016);
#12683=AXIS2_PLACEMENT_3D('',#19875,#16020,#16021);
#12684=AXIS2_PLACEMENT_3D('',#19881,#16025,#16026);
#12685=AXIS2_PLACEMENT_3D('',#19887,#16030,#16031);
#12686=AXIS2_PLACEMENT_3D('',#19890,#16034,#16035);
#12687=AXIS2_PLACEMENT_3D('',#19891,#16036,#16037);
#15962=DIRECTION('axis',(0.,0.,1.));
#15963=DIRECTION('refdir',(1.,0.,0.));
#15964=DIRECTION('center_axis',(0.,1.,0.));
#15965=DIRECTION('ref_axis',(0.,0.,1.));
#15966=DIRECTION('center_axis',(0.,-1.,0.));
#15967=DIRECTION('ref_axis',(1.,0.,0.));
#15968=DIRECTION('center_axis',(0.,-1.,0.));
#15969=DIRECTION('ref_axis',(1.,0.,0.));
#15970=DIRECTION('center_axis',(0.,-1.,0.));
#15971=DIRECTION('ref_axis',(1.,0.,0.));
#15972=DIRECTION('',(0.707106781186547,0.707106781186548,8.65956056235493E-17));
#15973=DIRECTION('center_axis',(0.,-1.,0.));
#15974=DIRECTION('ref_axis',(1.,0.,0.));
#15975=DIRECTION('center_axis',(0.,-1.,0.));
#15976=DIRECTION('ref_axis',(1.,0.,0.));
#15977=DIRECTION('',(0.,1.,0.));
#15978=DIRECTION('center_axis',(0.,1.,0.));
#15979=DIRECTION('ref_axis',(1.,0.,0.));
#15980=DIRECTION('center_axis',(0.,-1.,0.));
#15981=DIRECTION('ref_axis',(1.,0.,0.));
#15982=DIRECTION('',(-0.707106781186547,0.707106781186548,-8.65956056235493E-17));
#15983=DIRECTION('center_axis',(0.,-1.,0.));
#15984=DIRECTION('ref_axis',(0.,0.,-1.));
#15985=DIRECTION('center_axis',(0.,-1.,0.));
#15986=DIRECTION('ref_axis',(1.,0.,0.));
#15987=DIRECTION('center_axis',(0.,1.,0.));
#15988=DIRECTION('ref_axis',(1.,0.,0.));
#15989=DIRECTION('center_axis',(0.,1.,0.));
#15990=DIRECTION('ref_axis',(1.,0.,0.));
#15991=DIRECTION('',(-0.447213595499958,0.894427190999916,-5.47678698264203E-17));
#15992=DIRECTION('center_axis',(0.,-1.,0.));
#15993=DIRECTION('ref_axis',(1.,0.,0.));
#15994=DIRECTION('center_axis',(0.,1.,0.));
#15995=DIRECTION('ref_axis',(1.,0.,0.));
#15996=DIRECTION('',(0.,1.,0.));
#15997=DIRECTION('center_axis',(0.,1.,0.));
#15998=DIRECTION('ref_axis',(1.,0.,0.));
#15999=DIRECTION('center_axis',(0.,-1.,0.));
#16000=DIRECTION('ref_axis',(1.,0.,0.));
#16001=DIRECTION('',(-0.707106781186547,0.707106781186548,-8.65956056235493E-17));
#16002=DIRECTION('center_axis',(0.,-1.,0.));
#16003=DIRECTION('ref_axis',(0.,0.,-1.));
#16004=DIRECTION('center_axis',(0.866025403784439,0.,-0.5));
#16005=DIRECTION('ref_axis',(0.5,0.,0.866025403784439));
#16006=DIRECTION('',(-0.5,0.,-0.866025403784439));
#16007=DIRECTION('',(0.,-1.,0.));
#16008=DIRECTION('',(0.5,0.,0.866025403784439));
#16009=DIRECTION('',(0.,-1.,0.));
#16010=DIRECTION('center_axis',(1.60246890531964E-16,0.,-1.));
#16011=DIRECTION('ref_axis',(1.,0.,1.60246890531964E-16));
#16012=DIRECTION('',(-1.,0.,-1.60246890531964E-16));
#16013=DIRECTION('',(0.,-1.,0.));
#16014=DIRECTION('',(1.,0.,1.60246890531964E-16));
#16015=DIRECTION('center_axis',(-0.866025403784439,0.,-0.5));
#16016=DIRECTION('ref_axis',(0.5,0.,-0.866025403784439));
#16017=DIRECTION('',(-0.5,0.,0.866025403784439));
#16018=DIRECTION('',(0.,-1.,0.));
#16019=DIRECTION('',(0.5,0.,-0.866025403784439));
#16020=DIRECTION('center_axis',(-0.866025403784439,0.,0.5));
#16021=DIRECTION('ref_axis',(-0.5,0.,-0.866025403784439));
#16022=DIRECTION('',(0.5,0.,0.866025403784439));
#16023=DIRECTION('',(0.,-1.,0.));
#16024=DIRECTION('',(-0.5,0.,-0.866025403784439));
#16025=DIRECTION('center_axis',(-1.60246890531964E-16,0.,1.));
#16026=DIRECTION('ref_axis',(-1.,0.,-1.60246890531964E-16));
#16027=DIRECTION('',(1.,0.,1.60246890531964E-16));
#16028=DIRECTION('',(0.,-1.,0.));
#16029=DIRECTION('',(-1.,0.,-1.60246890531964E-16));
#16030=DIRECTION('center_axis',(0.866025403784439,0.,0.5));
#16031=DIRECTION('ref_axis',(-0.5,0.,0.866025403784439));
#16032=DIRECTION('',(0.5,0.,-0.866025403784439));
#16033=DIRECTION('',(-0.5,0.,0.866025403784439));
#16034=DIRECTION('center_axis',(0.,1.,0.));
#16035=DIRECTION('ref_axis',(1.,0.,0.));
#16036=DIRECTION('center_axis',(0.,-1.,0.));
#16037=DIRECTION('ref_axis',(0.,0.,-1.));
#19822=CARTESIAN_POINT('',(0.,0.,0.));
#19823=CARTESIAN_POINT('Origin',(0.3,0.4,0.));
#19824=CARTESIAN_POINT('',(-0.3,0.4,-3.67394039744206E-17));
#19825=CARTESIAN_POINT('Origin',(0.,0.4,0.));
#19826=CARTESIAN_POINT('Origin',(0.,0.375,0.));
#19827=CARTESIAN_POINT('',(-0.35,0.35,-4.28626379701573E-17));
#19828=CARTESIAN_POINT('Origin',(0.,0.35,0.));
#19829=CARTESIAN_POINT('',(-0.325,0.375,-3.9801020972289E-17));
#19830=CARTESIAN_POINT('Origin',(0.,0.19,0.));
#19831=CARTESIAN_POINT('',(-0.35,0.03,-4.28626379701574E-17));
#19832=CARTESIAN_POINT('Origin',(0.,0.03,0.));
#19833=CARTESIAN_POINT('',(-0.35,0.19,-4.28626379701574E-17));
#19834=CARTESIAN_POINT('Origin',(0.,0.0149999999999999,0.));
#19835=CARTESIAN_POINT('',(-0.32,-3.29597460435593E-17,-3.91886975727153E-17));
#19836=CARTESIAN_POINT('Origin',(0.,0.,0.));
#19837=CARTESIAN_POINT('',(-0.335,0.0149999999999999,-4.10256677714363E-17));
#19838=CARTESIAN_POINT('Origin',(0.22,0.,0.));
#19839=CARTESIAN_POINT('',(-0.22,-6.93889390390723E-18,-2.69422295812418E-17));
#19840=CARTESIAN_POINT('Origin',(0.,0.,0.));
#19841=CARTESIAN_POINT('Origin',(0.,-0.02,0.));
#19842=CARTESIAN_POINT('',(-0.1954,-0.0492,2.39295984553393E-17));
#19843=CARTESIAN_POINT('Origin',(0.,-0.0492,0.));
#19844=CARTESIAN_POINT('',(-0.21,-0.02,-2.57175827820944E-17));
#19845=CARTESIAN_POINT('Origin',(0.,-0.8,0.));
#19846=CARTESIAN_POINT('',(-0.1954,-1.5646,2.39295984553393E-17));
#19847=CARTESIAN_POINT('Origin',(0.,-1.5646,0.));
#19848=CARTESIAN_POINT('',(-0.1954,-0.8,-2.39295984553393E-17));
#19849=CARTESIAN_POINT('Origin',(0.,-1.58,0.));
#19850=CARTESIAN_POINT('',(-0.16,-1.6,-1.95943487863577E-17));
#19851=CARTESIAN_POINT('Origin',(0.,-1.6,0.));
#19852=CARTESIAN_POINT('',(-0.18,-1.58,-2.20436423846524E-17));
#19853=CARTESIAN_POINT('Origin',(0.,-1.6,0.));
#19854=CARTESIAN_POINT('Origin',(0.0866025403784439,-0.4,-0.15));
#19855=CARTESIAN_POINT('',(0.173205080756888,-0.4,0.));
#19856=CARTESIAN_POINT('',(0.0866025403784439,-0.4,-0.15));
#19857=CARTESIAN_POINT('',(0.173205080756888,-0.4,0.));
#19858=CARTESIAN_POINT('',(0.0866025403784439,-0.64,-0.15));
#19859=CARTESIAN_POINT('',(0.0866025403784439,-0.4,-0.15));
#19860=CARTESIAN_POINT('',(0.173205080756888,-0.64,0.));
#19861=CARTESIAN_POINT('',(0.173205080756888,-0.64,0.));
#19862=CARTESIAN_POINT('',(0.173205080756888,-0.4,0.));
#19863=CARTESIAN_POINT('Origin',(-0.0866025403784438,-0.4,-0.15));
#19864=CARTESIAN_POINT('',(-0.0866025403784438,-0.4,-0.15));
#19865=CARTESIAN_POINT('',(0.0866025403784439,-0.4,-0.15));
#19866=CARTESIAN_POINT('',(-0.0866025403784438,-0.64,-0.15));
#19867=CARTESIAN_POINT('',(-0.0866025403784438,-0.4,-0.15));
#19868=CARTESIAN_POINT('',(0.0866025403784439,-0.64,-0.15));
#19869=CARTESIAN_POINT('Origin',(-0.173205080756888,-0.4,-2.77555756156289E-17));
#19870=CARTESIAN_POINT('',(-0.173205080756888,-0.4,-2.12115047744981E-17));
#19871=CARTESIAN_POINT('',(-0.0866025403784438,-0.4,-0.15));
#19872=CARTESIAN_POINT('',(-0.173205080756888,-0.64,-2.77555756156289E-17));
#19873=CARTESIAN_POINT('',(-0.173205080756888,-0.4,-2.12115047744981E-17));
#19874=CARTESIAN_POINT('',(-0.0866025403784438,-0.64,-0.15));
#19875=CARTESIAN_POINT('Origin',(-0.0866025403784439,-0.4,0.15));
#19876=CARTESIAN_POINT('',(-0.0866025403784439,-0.4,0.15));
#19877=CARTESIAN_POINT('',(-0.173205080756888,-0.4,-2.12115047744981E-17));
#19878=CARTESIAN_POINT('',(-0.0866025403784439,-0.64,0.15));
#19879=CARTESIAN_POINT('',(-0.0866025403784439,-0.4,0.15));
#19880=CARTESIAN_POINT('',(-0.173205080756888,-0.64,-2.12115047744981E-17));
#19881=CARTESIAN_POINT('Origin',(0.0866025403784439,-0.4,0.15));
#19882=CARTESIAN_POINT('',(0.0866025403784439,-0.4,0.15));
#19883=CARTESIAN_POINT('',(-0.0866025403784439,-0.4,0.15));
#19884=CARTESIAN_POINT('',(0.0866025403784439,-0.64,0.15));
#19885=CARTESIAN_POINT('',(0.0866025403784439,-0.4,0.15));
#19886=CARTESIAN_POINT('',(-0.0866025403784439,-0.64,0.15));
#19887=CARTESIAN_POINT('Origin',(0.173205080756888,-0.4,0.));
#19888=CARTESIAN_POINT('',(0.0866025403784439,-0.4,0.15));
#19889=CARTESIAN_POINT('',(0.0866025403784439,-0.64,0.15));
#19890=CARTESIAN_POINT('Origin',(0.,-0.4,-2.77555756156289E-17));
#19891=CARTESIAN_POINT('Origin',(0.,-0.64,-2.77555756156289E-17));
#20041=UNCERTAINTY_MEASURE_WITH_UNIT(LENGTH_MEASURE(0.001),#20097,
'DISTANCE_ACCURACY_VALUE',
'Maximum model space distance between geometric entities at asserted c
onnectivities');
#20042=UNCERTAINTY_MEASURE_WITH_UNIT(LENGTH_MEASURE(0.001),#20097,
'DISTANCE_ACCURACY_VALUE',
'Maximum model space distance between geometric entities at asserted c
onnectivities');
#20095=(
GEOMETRIC_REPRESENTATION_CONTEXT(3)
GLOBAL_UNCERTAINTY_ASSIGNED_CONTEXT((#20041))
GLOBAL_UNIT_ASSIGNED_CONTEXT((#20097,#20099,#20100))
REPRESENTATION_CONTEXT('','3D')
);
#20096=(
GEOMETRIC_REPRESENTATION_CONTEXT(3)
GLOBAL_UNCERTAINTY_ASSIGNED_CONTEXT((#20042))
GLOBAL_UNIT_ASSIGNED_CONTEXT((#20097,#20099,#20100))
REPRESENTATION_CONTEXT('','3D')
);
#20097=(
LENGTH_UNIT()
NAMED_UNIT(*)
SI_UNIT(.CENTI.,.METRE.)
);
#20099=(
NAMED_UNIT(*)
PLANE_ANGLE_UNIT()
SI_UNIT($,.RADIAN.)
);
#20100=(
NAMED_UNIT(*)
SI_UNIT($,.STERADIAN.)
SOLID_ANGLE_UNIT()
);
#20153=SHAPE_DEFINITION_REPRESENTATION(#20214,#20364);
#20214=PRODUCT_DEFINITION_SHAPE('',$,#20418);
#20364=SHAPE_REPRESENTATION('',(#12662),#20095);
#20365=PRODUCT_DEFINITION_CONTEXT('part definition',#20526,'design');
#20418=PRODUCT_DEFINITION('Cap Screw - M4x16','Cap Screw - M4x16',#20471,
#20365);
#20471=PRODUCT_DEFINITION_FORMATION('',$,#20580);
#20526=APPLICATION_CONTEXT(
'Core Data for Automotive Mechanical Design Process');
#20527=PRODUCT_CONTEXT('part definition',#20526,'mechanical');
#20580=PRODUCT('Cap Screw - M4x16','Cap Screw - M4x16',
'Cap Screw - M4x16',(#20527));
#20651=COLOUR_RGB('Black',0.12,0.14,0.17);
#20652=FILL_AREA_STYLE_COLOUR('',#20651);
#20653=FILL_AREA_STYLE('',(#20652));
#20654=SURFACE_STYLE_FILL_AREA(#20653);
#20655=SURFACE_SIDE_STYLE('',(#20654));
#20656=SURFACE_STYLE_USAGE(.BOTH.,#20655);
#20657=PRESENTATION_STYLE_ASSIGNMENT((#20656));
ENDSEC;
END-ISO-10303-21;
